ISO-10303-21;
HEADER;
/* Generated by software containing ST-Developer
 * from STEP Tools, Inc. (www.steptools.com) 
 */

FILE_DESCRIPTION(
/* description */ ('XY cross-slide table'),
/* implementation_level */ '2;1');

FILE_NAME(
/* name */ 'Cap Screw - M4x16.step',
/* time_stamp */ '2026-10-28T03:22:46-07:00',
/* author */ (''),
/* organization */ (''),
/* preprocessor_version */ 'ST-DEVELOPER v20.2',
/* originating_system */ 'Autodesk Translation Framework v15.17.0.0',
/* authorisation */ '');

FILE_SCHEMA (('AUTOMOTIVE_DESIGN { 1 0 10303 214 3 1 1 }'));
ENDSEC;

DATA;
#10=MECHANICAL_DESIGN_GEOMETRIC_PRESENTATION_REPRESENTATION('',(#1715),#62984);
#20=ORIENTED_CLOSED_SHELL('',*,#23011,.F.);
#29=BREP_WITH_VOIDS('Body1',#23010,(#20));
#1453=CONICAL_SURFACE('',#24800,0.325,0.785398163397448);
#1454=CONICAL_SURFACE('',#24804,0.335,0.785398163397448);
#1455=CONICAL_SURFACE('',#24808,0.21,0.463647609000806);
#1456=CONICAL_SURFACE('',#24812,0.18,0.785398163397448);
#1534=SHAPE_REPRESENTATION_RELATIONSHIP('SRR','None',#63386,#1617);
#1617=ADVANCED_BREP_SHAPE_REPRESENTATION('',(#29),#62923);
#1715=STYLED_ITEM('',(#63919),#29);
#2059=FACE_BOUND('',#4751,.T.);
#2495=PLANE('',#24798);
#2496=PLANE('',#24806);
#2497=PLANE('',#24814);
#2498=PLANE('',#24815);
#2499=PLANE('',#24816);
#2500=PLANE('',#24817);
#2501=PLANE('',#24818);
#2502=PLANE('',#24819);
#2503=PLANE('',#24820);
#2504=PLANE('',#24821);
#2505=PLANE('',#24822);
#3260=FACE_OUTER_BOUND('',#4746,.T.);
#3261=FACE_OUTER_BOUND('',#4747,.T.);
#3262=FACE_OUTER_BOUND('',#4748,.T.);
#3263=FACE_OUTER_BOUND('',#4749,.T.);
#3264=FACE_OUTER_BOUND('',#4750,.T.);
#3265=FACE_OUTER_BOUND('',#4752,.T.);
#3266=FACE_OUTER_BOUND('',#4753,.T.);
#3267=FACE_OUTER_BOUND('',#4754,.T.);
#3268=FACE_OUTER_BOUND('',#4755,.T.);
#3269=FACE_OUTER_BOUND('',#4756,.T.);
#3270=FACE_OUTER_BOUND('',#4757,.T.);
#3271=FACE_OUTER_BOUND('',#4758,.T.);
#3272=FACE_OUTER_BOUND('',#4759,.T.);
#3273=FACE_OUTER_BOUND('',#4760,.T.);
#3274=FACE_OUTER_BOUND('',#4761,.T.);
#3275=FACE_OUTER_BOUND('',#4762,.T.);
#3276=FACE_OUTER_BOUND('',#4763,.T.);
#4746=EDGE_LOOP('',(#16670));
#4747=EDGE_LOOP('',(#16671,#16672,#16673,#16674));
#4748=EDGE_LOOP('',(#16675,#16676,#16677,#16678));
#4749=EDGE_LOOP('',(#16679,#16680,#16681,#16682));
#4750=EDGE_LOOP('',(#16683));
#4751=EDGE_LOOP('',(#16684));
#4752=EDGE_LOOP('',(#16685,#16686,#16687,#16688));
#4753=EDGE_LOOP('',(#16689,#16690,#16691,#16692));
#4754=EDGE_LOOP('',(#16693,#16694,#16695,#16696));
#4755=EDGE_LOOP('',(#16697));
#4756=EDGE_LOOP('',(#16698,#16699,#16700,#16701));
#4757=EDGE_LOOP('',(#16702,#16703,#16704,#16705));
#4758=EDGE_LOOP('',(#16706,#16707,#16708,#16709));
#4759=EDGE_LOOP('',(#16710,#16711,#16712,#16713));
#4760=EDGE_LOOP('',(#16714,#16715,#16716,#16717));
#4761=EDGE_LOOP('',(#16718,#16719,#16720,#16721));
#4762=EDGE_LOOP('',(#16722,#16723,#16724,#16725,#16726,#16727));
#4763=EDGE_LOOP('',(#16728,#16729,#16730,#16731,#16732,#16733));
#6356=LINE('',#37464,#7843);
#6357=LINE('',#37468,#7844);
#6358=LINE('',#37472,#7845);
#6359=LINE('',#37479,#7846);
#6360=LINE('',#37483,#7847);
#6361=LINE('',#37487,#7848);
#6362=LINE('',#37492,#7849);
#6363=LINE('',#37494,#7850);
#6364=LINE('',#37496,#7851);
#6365=LINE('',#37497,#7852);
#6366=LINE('',#37500,#7853);
#6367=LINE('',#37502,#7854);
#6368=LINE('',#37503,#7855);
#6369=LINE('',#37506,#7856);
#6370=LINE('',#37508,#7857);
#6371=LINE('',#37509,#7858);
#6372=LINE('',#37512,#7859);
#6373=LINE('',#37514,#7860);
#6374=LINE('',#37515,#7861);
#6375=LINE('',#37518,#7862);
#6376=LINE('',#37520,#7863);
#6377=LINE('',#37521,#7864);
#6378=LINE('',#37523,#7865);
#6379=LINE('',#37524,#7866);
#7843=VECTOR('',#28515,0.325);
#7844=VECTOR('',#28520,0.35);
#7845=VECTOR('',#28525,0.335);
#7846=VECTOR('',#28534,0.21);
#7847=VECTOR('',#28539,0.2);
#7848=VECTOR('',#28544,0.18);
#7849=VECTOR('',#28549,1.);
#7850=VECTOR('',#28550,1.);
#7851=VECTOR('',#28551,1.);
#7852=VECTOR('',#28552,1.);
#7853=VECTOR('',#28555,1.);
#7854=VECTOR('',#28556,1.);
#7855=VECTOR('',#28557,1.);
#7856=VECTOR('',#28560,1.);
#7857=VECTOR('',#28561,1.);
#7858=VECTOR('',#28562,1.);
#7859=VECTOR('',#28565,1.);
#7860=VECTOR('',#28566,1.);
#7861=VECTOR('',#28567,1.);
#7862=VECTOR('',#28570,1.);
#7863=VECTOR('',#28571,1.);
#7864=VECTOR('',#28572,1.);
#7865=VECTOR('',#28575,1.);
#7866=VECTOR('',#28576,1.);
#9238=CIRCLE('',#24799,0.3);
#9239=CIRCLE('',#24801,0.35);
#9240=CIRCLE('',#24803,0.35);
#9241=CIRCLE('',#24805,0.32);
#9242=CIRCLE('',#24807,0.22);
#9243=CIRCLE('',#24809,0.1954);
#9244=CIRCLE('',#24811,0.1954);
#9245=CIRCLE('',#24813,0.16);
#10375=VERTEX_POINT('',#37459);
#10376=VERTEX_POINT('',#37462);
#10377=VERTEX_POINT('',#37466);
#10378=VERTEX_POINT('',#37470);
#10379=VERTEX_POINT('',#37474);
#10380=VERTEX_POINT('',#37477);
#10381=VERTEX_POINT('',#37481);
#10382=VERTEX_POINT('',#37485);
#10383=VERTEX_POINT('',#37490);
#10384=VERTEX_POINT('',#37491);
#10385=VERTEX_POINT('',#37493);
#10386=VERTEX_POINT('',#37495);
#10387=VERTEX_POINT('',#37499);
#10388=VERTEX_POINT('',#37501);
#10389=VERTEX_POINT('',#37505);
#10390=VERTEX_POINT('',#37507);
#10391=VERTEX_POINT('',#37511);
#10392=VERTEX_POINT('',#37513);
#10393=VERTEX_POINT('',#37517);
#10394=VERTEX_POINT('',#37519);
#12719=EDGE_CURVE('',#10375,#10375,#9238,.T.);
#12720=EDGE_CURVE('',#10376,#10376,#9239,.T.);
#12721=EDGE_CURVE('',#10376,#10375,#6356,.T.);
#12722=EDGE_CURVE('',#10377,#10377,#9240,.T.);
#12723=EDGE_CURVE('',#10377,#10376,#6357,.T.);
#12724=EDGE_CURVE('',#10378,#10378,#9241,.T.);
#12725=EDGE_CURVE('',#10378,#10377,#6358,.T.);
#12726=EDGE_CURVE('',#10379,#10379,#9242,.T.);
#12727=EDGE_CURVE('',#10380,#10380,#9243,.F.);
#12728=EDGE_CURVE('',#10380,#10379,#6359,.T.);
#12729=EDGE_CURVE('',#10381,#10381,#9244,.F.);
#12730=EDGE_CURVE('',#10381,#10380,#6360,.T.);
#12731=EDGE_CURVE('',#10382,#10382,#9245,.T.);
#12732=EDGE_CURVE('',#10382,#10381,#6361,.T.);
#12733=EDGE_CURVE('',#10383,#10384,#6362,.T.);
#12734=EDGE_CURVE('',#10384,#10385,#6363,.T.);
#12735=EDGE_CURVE('',#10385,#10386,#6364,.T.);
#12736=EDGE_CURVE('',#10383,#10386,#6365,.T.);
#12737=EDGE_CURVE('',#10384,#10387,#6366,.T.);
#12738=EDGE_CURVE('',#10387,#10388,#6367,.T.);
#12739=EDGE_CURVE('',#10388,#10385,#6368,.T.);
#12740=EDGE_CURVE('',#10387,#10389,#6369,.T.);
#12741=EDGE_CURVE('',#10389,#10390,#6370,.T.);
#12742=EDGE_CURVE('',#10390,#10388,#6371,.T.);
#12743=EDGE_CURVE('',#10389,#10391,#6372,.T.);
#12744=EDGE_CURVE('',#10391,#10392,#6373,.T.);
#12745=EDGE_CURVE('',#10392,#10390,#6374,.T.);
#12746=EDGE_CURVE('',#10391,#10393,#6375,.T.);
#12747=EDGE_CURVE('',#10393,#10394,#6376,.T.);
#12748=EDGE_CURVE('',#10394,#10392,#6377,.T.);
#12749=EDGE_CURVE('',#10393,#10383,#6378,.T.);
#12750=EDGE_CURVE('',#10386,#10394,#6379,.T.);
#16670=ORIENTED_EDGE('',*,*,#12719,.F.);
#16671=ORIENTED_EDGE('',*,*,#12720,.F.);
#16672=ORIENTED_EDGE('',*,*,#12721,.T.);
#16673=ORIENTED_EDGE('',*,*,#12719,.T.);
#16674=ORIENTED_EDGE('',*,*,#12721,.F.);
#16675=ORIENTED_EDGE('',*,*,#12722,.F.);
#16676=ORIENTED_EDGE('',*,*,#12723,.T.);
#16677=ORIENTED_EDGE('',*,*,#12720,.T.);
#16678=ORIENTED_EDGE('',*,*,#12723,.F.);
#16679=ORIENTED_EDGE('',*,*,#12724,.F.);
#16680=ORIENTED_EDGE('',*,*,#12725,.T.);
#16681=ORIENTED_EDGE('',*,*,#12722,.T.);
#16682=ORIENTED_EDGE('',*,*,#12725,.F.);
#16683=ORIENTED_EDGE('',*,*,#12724,.T.);
#16684=ORIENTED_EDGE('',*,*,#12726,.F.);
#16685=ORIENTED_EDGE('',*,*,#12727,.F.);
#16686=ORIENTED_EDGE('',*,*,#12728,.T.);
#16687=ORIENTED_EDGE('',*,*,#12726,.T.);
#16688=ORIENTED_EDGE('',*,*,#12728,.F.);
#16689=ORIENTED_EDGE('',*,*,#12729,.F.);
#16690=ORIENTED_EDGE('',*,*,#12730,.T.);
#16691=ORIENTED_EDGE('',*,*,#12727,.T.);
#16692=ORIENTED_EDGE('',*,*,#12730,.F.);
#16693=ORIENTED_EDGE('',*,*,#12731,.F.);
#16694=ORIENTED_EDGE('',*,*,#12732,.T.);
#16695=ORIENTED_EDGE('',*,*,#12729,.T.);
#16696=ORIENTED_EDGE('',*,*,#12732,.F.);
#16697=ORIENTED_EDGE('',*,*,#12731,.T.);
#16698=ORIENTED_EDGE('',*,*,#12733,.T.);
#16699=ORIENTED_EDGE('',*,*,#12734,.T.);
#16700=ORIENTED_EDGE('',*,*,#12735,.T.);
#16701=ORIENTED_EDGE('',*,*,#12736,.F.);
#16702=ORIENTED_EDGE('',*,*,#12737,.T.);
#16703=ORIENTED_EDGE('',*,*,#12738,.T.);
#16704=ORIENTED_EDGE('',*,*,#12739,.T.);
#16705=ORIENTED_EDGE('',*,*,#12734,.F.);
#16706=ORIENTED_EDGE('',*,*,#12740,.T.);
#16707=ORIENTED_EDGE('',*,*,#12741,.T.);
#16708=ORIENTED_EDGE('',*,*,#12742,.T.);
#16709=ORIENTED_EDGE('',*,*,#12738,.F.);
#16710=ORIENTED_EDGE('',*,*,#12743,.T.);
#16711=ORIENTED_EDGE('',*,*,#12744,.T.);
#16712=ORIENTED_EDGE('',*,*,#12745,.T.);
#16713=ORIENTED_EDGE('',*,*,#12741,.F.);
#16714=ORIENTED_EDGE('',*,*,#12746,.T.);
#16715=ORIENTED_EDGE('',*,*,#12747,.T.);
#16716=ORIENTED_EDGE('',*,*,#12748,.T.);
#16717=ORIENTED_EDGE('',*,*,#12744,.F.);
#16718=ORIENTED_EDGE('',*,*,#12749,.T.);
#16719=ORIENTED_EDGE('',*,*,#12736,.T.);
#16720=ORIENTED_EDGE('',*,*,#12750,.T.);
#16721=ORIENTED_EDGE('',*,*,#12747,.F.);
#16722=ORIENTED_EDGE('',*,*,#12749,.F.);
#16723=ORIENTED_EDGE('',*,*,#12746,.F.);
#16724=ORIENTED_EDGE('',*,*,#12743,.F.);
#16725=ORIENTED_EDGE('',*,*,#12740,.F.);
#16726=ORIENTED_EDGE('',*,*,#12737,.F.);
#16727=ORIENTED_EDGE('',*,*,#12733,.F.);
#16728=ORIENTED_EDGE('',*,*,#12750,.F.);
#16729=ORIENTED_EDGE('',*,*,#12735,.F.);
#16730=ORIENTED_EDGE('',*,*,#12739,.F.);
#16731=ORIENTED_EDGE('',*,*,#12742,.F.);
#16732=ORIENTED_EDGE('',*,*,#12745,.F.);
#16733=ORIENTED_EDGE('',*,*,#12748,.F.);
#21184=CYLINDRICAL_SURFACE('',#24802,0.35);
#21185=CYLINDRICAL_SURFACE('',#24810,0.1954);
#22041=ADVANCED_FACE('',(#3260),#2495,.T.);
#22042=ADVANCED_FACE('',(#3261),#1453,.T.);
#22043=ADVANCED_FACE('',(#3262),#21184,.T.);
#22044=ADVANCED_FACE('',(#3263),#1454,.T.);
#22045=ADVANCED_FACE('',(#3264,#2059),#2496,.T.);
#22046=ADVANCED_FACE('',(#3265),#1455,.T.);
#22047=ADVANCED_FACE('',(#3266),#21185,.T.);
#22048=ADVANCED_FACE('',(#3267),#1456,.T.);
#22049=ADVANCED_FACE('',(#3268),#2497,.T.);
#22050=ADVANCED_FACE('',(#3269),#2498,.F.);
#22051=ADVANCED_FACE('',(#3270),#2499,.F.);
#22052=ADVANCED_FACE('',(#3271),#2500,.F.);
#22053=ADVANCED_FACE('',(#3272),#2501,.F.);
#22054=ADVANCED_FACE('',(#3273),#2502,.F.);
#22055=ADVANCED_FACE('',(#3274),#2503,.F.);
#22056=ADVANCED_FACE('',(#3275),#2504,.F.);
#22057=ADVANCED_FACE('',(#3276),#2505,.F.);
#23010=CLOSED_SHELL('',(#22041,#22042,#22043,#22044,#22045,#22046,#22047,
#22048,#22049));
#23011=CLOSED_SHELL('',(#22050,#22051,#22052,#22053,#22054,#22055,#22056,
#22057));
#24797=AXIS2_PLACEMENT_3D('',#37457,#28505,#28506);
#24798=AXIS2_PLACEMENT_3D('',#37458,#28507,#28508);
#24799=AXIS2_PLACEMENT_3D('',#37460,#28509,#28510);
#24800=AXIS2_PLACEMENT_3D('',#37461,#28511,#28512);
#24801=AXIS2_PLACEMENT_3D('',#37463,#28513,#28514);
#24802=AXIS2_PLACEMENT_3D('',#37465,#28516,#28517);
#24803=AXIS2_PLACEMENT_3D('',#37467,#28518,#28519);
#24804=AXIS2_PLACEMENT_3D('',#37469,#28521,#28522);
#24805=AXIS2_PLACEMENT_3D('',#37471,#28523,#28524);
#24806=AXIS2_PLACEMENT_3D('',#37473,#28526,#28527);
#24807=AXIS2_PLACEMENT_3D('',#37475,#28528,#28529);
#24808=AXIS2_PLACEMENT_3D('',#37476,#28530,#28531);
#24809=AXIS2_PLACEMENT_3D('',#37478,#28532,#28533);
#24810=AXIS2_PLACEMENT_3D('',#37480,#28535,#28536);
#24811=AXIS2_PLACEMENT_3D('',#37482,#28537,#28538);
#24812=AXIS2_PLACEMENT_3D('',#37484,#28540,#28541);
#24813=AXIS2_PLACEMENT_3D('',#37486,#28542,#28543);
#24814=AXIS2_PLACEMENT_3D('',#37488,#28545,#28546);
#24815=AXIS2_PLACEMENT_3D('',#37489,#28547,#28548);
#24816=AXIS2_PLACEMENT_3D('',#37498,#28553,#28554);
#24817=AXIS2_PLACEMENT_3D('',#37504,#28558,#28559);
#24818=AXIS2_PLACEMENT_3D('',#37510,#28563,#28564);
#24819=AXIS2_PLACEMENT_3D('',#37516,#28568,#28569);
#24820=AXIS2_PLACEMENT_3D('',#37522,#28573,#28574);
#24821=AXIS2_PLACEMENT_3D('',#37525,#28577,#28578);
#24822=AXIS2_PLACEMENT_3D('',#37526,#28579,#28580);
#28505=DIRECTION('axis',(0.,0.,1.));
#28506=DIRECTION('refdir',(1.,0.,0.));
#28507=DIRECTION('center_axis',(0.,1.,0.));
#28508=DIRECTION('ref_axis',(0.,0.,1.));
#28509=DIRECTION('center_axis',(0.,-1.,0.));
#28510=DIRECTION('ref_axis',(1.,0.,0.));
#28511=DIRECTION('center_axis',(0.,-1.,0.));
#28512=DIRECTION('ref_axis',(1.,0.,0.));
#28513=DIRECTION('center_axis',(0.,-1.,0.));
#28514=DIRECTION('ref_axis',(1.,0.,0.));
#28515=DIRECTION('',(0.707106781186547,0.707106781186548,8.65956056235493E-17));
#28516=DIRECTION('center_axis',(0.,-1.,0.));
#28517=DIRECTION('ref_axis',(1.,0.,0.));
#28518=DIRECTION('center_axis',(0.,-1.,0.));
#28519=DIRECTION('ref_axis',(1.,0.,0.));
#28520=DIRECTION('',(0.,1.,0.));
#28521=DIRECTION('center_axis',(0.,1.,0.));
#28522=DIRECTION('ref_axis',(1.,0.,0.));
#28523=DIRECTION('center_axis',(0.,-1.,0.));
#28524=DIRECTION('ref_axis',(1.,0.,0.));
#28525=DIRECTION('',(-0.707106781186547,0.707106781186548,-8.65956056235493E-17));
#28526=DIRECTION('center_axis',(0.,-1.,0.));
#28527=DIRECTION('ref_axis',(0.,0.,-1.));
#28528=DIRECTION('center_axis',(0.,-1.,0.));
#28529=DIRECTION('ref_axis',(1.,0.,0.));
#28530=DIRECTION('center_axis',(0.,1.,0.));
#28531=DIRECTION('ref_axis',(1.,0.,0.));
#28532=DIRECTION('center_axis',(0.,1.,0.));
#28533=DIRECTION('ref_axis',(1.,0.,0.));
#28534=DIRECTION('',(-0.447213595499958,0.894427190999916,-5.47678698264203E-17));
#28535=DIRECTION('center_axis',(0.,-1.,0.));
#28536=DIRECTION('ref_axis',(1.,0.,0.));
#28537=DIRECTION('center_axis',(0.,1.,0.));
#28538=DIRECTION('ref_axis',(1.,0.,0.));
#28539=DIRECTION('',(0.,1.,0.));
#28540=DIRECTION('center_axis',(0.,1.,0.));
#28541=DIRECTION('ref_axis',(1.,0.,0.));
#28542=DIRECTION('center_axis',(0.,-1.,0.));
#28543=DIRECTION('ref_axis',(1.,0.,0.));
#28544=DIRECTION('',(-0.707106781186547,0.707106781186548,-8.65956056235493E-17));
#28545=DIRECTION('center_axis',(0.,-1.,0.));
#28546=DIRECTION('ref_axis',(0.,0.,-1.));
#28547=DIRECTION('center_axis',(0.866025403784439,0.,-0.5));
#28548=DIRECTION('ref_axis',(0.5,0.,0.866025403784439));
#28549=DIRECTION('',(-0.5,0.,-0.866025403784439));
#28550=DIRECTION('',(0.,-1.,0.));
#28551=DIRECTION('',(0.5,0.,0.866025403784439));
#28552=DIRECTION('',(0.,-1.,0.));
#28553=DIRECTION('center_axis',(1.60246890531964E-16,0.,-1.));
#28554=DIRECTION('ref_axis',(1.,0.,1.60246890531964E-16));
#28555=DIRECTION('',(-1.,0.,-1.60246890531964E-16));
#28556=DIRECTION('',(0.,-1.,0.));
#28557=DIRECTION('',(1.,0.,1.60246890531964E-16));
#28558=DIRECTION('center_axis',(-0.866025403784439,0.,-0.5));
#28559=DIRECTION('ref_axis',(0.5,0.,-0.866025403784439));
#28560=DIRECTION('',(-0.5,0.,0.866025403784439));
#28561=DIRECTION('',(0.,-1.,0.));
#28562=DIRECTION('',(0.5,0.,-0.866025403784439));
#28563=DIRECTION('center_axis',(-0.866025403784439,0.,0.5));
#28564=DIRECTION('ref_axis',(-0.5,0.,-0.866025403784439));
#28565=DIRECTION('',(0.5,0.,0.866025403784439));
#28566=DIRECTION('',(0.,-1.,0.));
#28567=DIRECTION('',(-0.5,0.,-0.866025403784439));
#28568=DIRECTION('center_axis',(-1.60246890531964E-16,0.,1.));
#28569=DIRECTION('ref_axis',(-1.,0.,-1.60246890531964E-16));
#28570=DIRECTION('',(1.,0.,1.60246890531964E-16));
#28571=DIRECTION('',(0.,-1.,0.));
#28572=DIRECTION('',(-1.,0.,-1.60246890531964E-16));
#28573=DIRECTION('center_axis',(0.866025403784439,0.,0.5));
#28574=DIRECTION('ref_axis',(-0.5,0.,0.866025403784439));
#28575=DIRECTION('',(0.5,0.,-0.866025403784439));
#28576=DIRECTION('',(-0.5,0.,0.866025403784439));
#28577=DIRECTION('center_axis',(0.,1.,0.));
#28578=DIRECTION('ref_axis',(1.,0.,0.));
#28579=DIRECTION('center_axis',(0.,-1.,0.));
#28580=DIRECTION('ref_axis',(0.,0.,-1.));
#37457=CARTESIAN_POINT('',(0.,0.,0.));
#37458=CARTESIAN_POINT('Origin',(0.3,0.4,0.));
#37459=CARTESIAN_POINT('',(-0.3,0.4,-3.67394039744206E-17));
#37460=CARTESIAN_POINT('Origin',(0.,0.4,0.));
#37461=CARTESIAN_POINT('Origin',(0.,0.375,0.));
#37462=CARTESIAN_POINT('',(-0.35,0.35,-4.28626379701573E-17));
#37463=CARTESIAN_POINT('Origin',(0.,0.35,0.));
#37464=CARTESIAN_POINT('',(-0.325,0.375,-3.9801020972289E-17));
#37465=CARTESIAN_POINT('Origin',(0.,0.19,0.));
#37466=CARTESIAN_POINT('',(-0.35,0.03,-4.28626379701574E-17));
#37467=CARTESIAN_POINT('Origin',(0.,0.03,0.));
#37468=CARTESIAN_POINT('',(-0.35,0.19,-4.28626379701574E-17));
#37469=CARTESIAN_POINT('Origin',(0.,0.0149999999999999,0.));
#37470=CARTESIAN_POINT('',(-0.32,-3.29597460435593E-17,-3.91886975727153E-17));
#37471=CARTESIAN_POINT('Origin',(0.,0.,0.));
#37472=CARTESIAN_POINT('',(-0.335,0.0149999999999999,-4.10256677714363E-17));
#37473=CARTESIAN_POINT('Origin',(0.22,0.,0.));
#37474=CARTESIAN_POINT('',(-0.22,-6.93889390390723E-18,-2.69422295812418E-17));
#37475=CARTESIAN_POINT('Origin',(0.,0.,0.));
#37476=CARTESIAN_POINT('Origin',(0.,-0.02,0.));
#37477=CARTESIAN_POINT('',(-0.1954,-0.0492,2.39295984553393E-17));
#37478=CARTESIAN_POINT('Origin',(0.,-0.0492,0.));
#37479=CARTESIAN_POINT('',(-0.21,-0.02,-2.57175827820944E-17));
#37480=CARTESIAN_POINT('Origin',(0.,-0.8,0.));
#37481=CARTESIAN_POINT('',(-0.1954,-1.5646,2.39295984553393E-17));
#37482=CARTESIAN_POINT('Origin',(0.,-1.5646,0.));
#37483=CARTESIAN_POINT('',(-0.1954,-0.8,-2.39295984553393E-17));
#37484=CARTESIAN_POINT('Origin',(0.,-1.58,0.));
#37485=CARTESIAN_POINT('',(-0.16,-1.6,-1.95943487863577E-17));
#37486=CARTESIAN_POINT('Origin',(0.,-1.6,0.));
#37487=CARTESIAN_POINT('',(-0.18,-1.58,-2.20436423846524E-17));
#37488=CARTESIAN_POINT('Origin',(0.,-1.6,0.));
#37489=CARTESIAN_POINT('Origin',(0.0866025403784439,-0.4,-0.15));
#37490=CARTESIAN_POINT('',(0.173205080756888,-0.4,0.));
#37491=CARTESIAN_POINT('',(0.0866025403784439,-0.4,-0.15));
#37492=CARTESIAN_POINT('',(0.173205080756888,-0.4,0.));
#37493=CARTESIAN_POINT('',(0.0866025403784439,-0.64,-0.15));
#37494=CARTESIAN_POINT('',(0.0866025403784439,-0.4,-0.15));
#37495=CARTESIAN_POINT('',(0.173205080756888,-0.64,0.));
#37496=CARTESIAN_POINT('',(0.173205080756888,-0.64,0.));
#37497=CARTESIAN_POINT('',(0.173205080756888,-0.4,0.));
#37498=CARTESIAN_POINT('Origin',(-0.0866025403784438,-0.4,-0.15));
#37499=CARTESIAN_POINT('',(-0.0866025403784438,-0.4,-0.15));
#37500=CARTESIAN_POINT('',(0.0866025403784439,-0.4,-0.15));
#37501=CARTESIAN_POINT('',(-0.0866025403784438,-0.64,-0.15));
#37502=CARTESIAN_POINT('',(-0.0866025403784438,-0.4,-0.15));
#37503=CARTESIAN_POINT('',(0.0866025403784439,-0.64,-0.15));
#37504=CARTESIAN_POINT('Origin',(-0.173205080756888,-0.4,-2.77555756156289E-17));
#37505=CARTESIAN_POINT('',(-0.173205080756888,-0.4,-2.12115047744981E-17));
#37506=CARTESIAN_POINT('',(-0.0866025403784438,-0.4,-0.15));
#37507=CARTESIAN_POINT('',(-0.173205080756888,-0.64,-2.77555756156289E-17));
#37508=CARTESIAN_POINT('',(-0.173205080756888,-0.4,-2.12115047744981E-17));
#37509=CARTESIAN_POINT('',(-0.0866025403784438,-0.64,-0.15));
#37510=CARTESIAN_POINT('Origin',(-0.0866025403784439,-0.4,0.15));
#37511=CARTESIAN_POINT('',(-0.0866025403784439,-0.4,0.15));
#37512=CARTESIAN_POINT('',(-0.173205080756888,-0.4,-2.12115047744981E-17));
#37513=CARTESIAN_POINT('',(-0.0866025403784439,-0.64,0.15));
#37514=CARTESIAN_POINT('',(-0.0866025403784439,-0.4,0.15));
#37515=CARTESIAN_POINT('',(-0.173205080756888,-0.64,-2.12115047744981E-17));
#37516=CARTESIAN_POINT('Origin',(0.0866025403784439,-0.4,0.15));
#37517=CARTESIAN_POINT('',(0.0866025403784439,-0.4,0.15));
#37518=CARTESIAN_POINT('',(-0.0866025403784439,-0.4,0.15));
#37519=CARTESIAN_POINT('',(0.0866025403784439,-0.64,0.15));
#37520=CARTESIAN_POINT('',(0.0866025403784439,-0.4,0.15));
#37521=CARTESIAN_POINT('',(-0.0866025403784439,-0.64,0.15));
#37522=CARTESIAN_POINT('Origin',(0.173205080756888,-0.4,0.));
#37523=CARTESIAN_POINT('',(0.0866025403784439,-0.4,0.15));
#37524=CARTESIAN_POINT('',(0.0866025403784439,-0.64,0.15));
#37525=CARTESIAN_POINT('Origin',(0.,-0.4,-2.77555756156289E-17));
#37526=CARTESIAN_POINT('Origin',(0.,-0.64,-2.77555756156289E-17));
#62824=UNCERTAINTY_MEASURE_WITH_UNIT(LENGTH_MEASURE(0.001),#62985,
'DISTANCE_ACCURACY_VALUE',
'Maximum model space distance between geometric entities at asserted c
onnectivities');
#62885=UNCERTAINTY_MEASURE_WITH_UNIT(LENGTH_MEASURE(0.001),#62985,
'DISTANCE_ACCURACY_VALUE',
'Maximum model space distance between geometric entities at asserted c
onnectivities');
#62923=(
GEOMETRIC_REPRESENTATION_CONTEXT(3)
GLOBAL_UNCERTAINTY_ASSIGNED_CONTEXT((#62824))
GLOBAL_UNIT_ASSIGNED_CONTEXT((#62985,#62987,#62988))
REPRESENTATION_CONTEXT('','3D')
);
#62984=(
GEOMETRIC_REPRESENTATION_CONTEXT(3)
GLOBAL_UNCERTAINTY_ASSIGNED_CONTEXT((#62885))
GLOBAL_UNIT_ASSIGNED_CONTEXT((#62985,#62987,#62988))
REPRESENTATION_CONTEXT('','3D')
);
#62985=(
LENGTH_UNIT()
NAMED_UNIT(*)
SI_UNIT(.CENTI.,.METRE.)
);
#62987=(
NAMED_UNIT(*)
PLANE_ANGLE_UNIT()
SI_UNIT($,.RADIAN.)
);
#62988=(
NAMED_UNIT(*)
SI_UNIT($,.STERADIAN.)
SOLID_ANGLE_UNIT()
);
#63026=SHAPE_DEFINITION_REPRESENTATION(#63137,#63386);
#63137=PRODUCT_DEFINITION_SHAPE('',$,#63485);
#63386=SHAPE_REPRESENTATION('',(#24797),#62923);
#63447=PRODUCT_DEFINITION_CONTEXT('part definition',#63743,'design');
#63485=PRODUCT_DEFINITION('Cap Screw - M4x16','Cap Screw - M4x16',#63583,
#63447);
#63583=PRODUCT_DEFINITION_FORMATION('',$,#63782);
#63743=APPLICATION_CONTEXT(
'Core Data for Automotive Mechanical Design Process');
#63744=PRODUCT_CONTEXT('part definition',#63743,'mechanical');
#63782=PRODUCT('Cap Screw - M4x16','Cap Screw - M4x16',
'Cap Screw - M4x16',(#63744));
#63913=COLOUR_RGB('Black',0.12,0.14,0.17);
#63914=FILL_AREA_STYLE_COLOUR('',#63913);
#63915=FILL_AREA_STYLE('',(#63914));
#63916=SURFACE_STYLE_FILL_AREA(#63915);
#63917=SURFACE_SIDE_STYLE('',(#63916));
#63918=SURFACE_STYLE_USAGE(.BOTH.,#63917);
#63919=PRESENTATION_STYLE_ASSIGNMENT((#63918));
ENDSEC;
END-ISO-10303-21;
